ISO-10303-21;
HEADER;
/* Generated by software containing ST-Developer
 * from STEP Tools, Inc. (www.steptools.com) 
 */

FILE_DESCRIPTION(
/* description */ ('PAT-091'),
/* implementation_level */ '2;1');

FILE_NAME(
/* name */ 'Bearing inner spacer (1).step',
/* time_stamp */ '2026-10-27T15:34:44-07:00',
/* author */ (''),
/* organization */ (''),
/* preprocessor_version */ 'ST-DEVELOPER v20.2',
/* originating_system */ 'Autodesk Translation Framework v15.17.0.0',
/* authorisation */ '');

FILE_SCHEMA (('AUTOMOTIVE_DESIGN { 1 0 10303 214 3 1 1 }'));
ENDSEC;

DATA;
#10=MECHANICAL_DESIGN_GEOMETRIC_PRESENTATION_REPRESENTATION('',(#1090),#25100);
#857=SHAPE_REPRESENTATION_RELATIONSHIP('SRR','None',#25626,#967);
#967=ADVANCED_BREP_SHAPE_REPRESENTATION('',(#1211),#25096);
#1090=STYLED_ITEM('',(#26191),#1211);
#1211=MANIFOLD_SOLID_BREP('Body1',#13370);
#1631=FACE_BOUND('',#4100,.T.);
#1632=FACE_BOUND('',#4102,.T.);
#2054=PLANE('',#16421);
#2055=PLANE('',#16422);
#2863=FACE_OUTER_BOUND('',#4097,.T.);
#2864=FACE_OUTER_BOUND('',#4098,.T.);
#2865=FACE_OUTER_BOUND('',#4099,.T.);
#2866=FACE_OUTER_BOUND('',#4101,.T.);
#4097=EDGE_LOOP('',(#12020,#12021,#12022,#12023));
#4098=EDGE_LOOP('',(#12024,#12025,#12026,#12027));
#4099=EDGE_LOOP('',(#12028));
#4100=EDGE_LOOP('',(#12029));
#4101=EDGE_LOOP('',(#12030));
#4102=EDGE_LOOP('',(#12031));
#4855=LINE('',#24783,#5595);
#4856=LINE('',#24789,#5596);
#5595=VECTOR('',#20863,0.605);
#5596=VECTOR('',#20870,0.8);
#6365=CIRCLE('',#16416,0.605);
#6366=CIRCLE('',#16417,0.605);
#6367=CIRCLE('',#16419,0.8);
#6368=CIRCLE('',#16420,0.8);
#7403=VERTEX_POINT('',#24780);
#7404=VERTEX_POINT('',#24782);
#7405=VERTEX_POINT('',#24786);
#7406=VERTEX_POINT('',#24788);
#8945=EDGE_CURVE('',#7403,#7403,#6365,.T.);
#8946=EDGE_CURVE('',#7403,#7404,#4855,.T.);
#8947=EDGE_CURVE('',#7404,#7404,#6366,.T.);
#8948=EDGE_CURVE('',#7405,#7405,#6367,.T.);
#8949=EDGE_CURVE('',#7405,#7406,#4856,.T.);
#8950=EDGE_CURVE('',#7406,#7406,#6368,.T.);
#12020=ORIENTED_EDGE('',*,*,#8945,.F.);
#12021=ORIENTED_EDGE('',*,*,#8946,.T.);
#12022=ORIENTED_EDGE('',*,*,#8947,.T.);
#12023=ORIENTED_EDGE('',*,*,#8946,.F.);
#12024=ORIENTED_EDGE('',*,*,#8948,.F.);
#12025=ORIENTED_EDGE('',*,*,#8949,.T.);
#12026=ORIENTED_EDGE('',*,*,#8950,.T.);
#12027=ORIENTED_EDGE('',*,*,#8949,.F.);
#12028=ORIENTED_EDGE('',*,*,#8948,.T.);
#12029=ORIENTED_EDGE('',*,*,#8945,.T.);
#12030=ORIENTED_EDGE('',*,*,#8950,.F.);
#12031=ORIENTED_EDGE('',*,*,#8947,.F.);
#12421=CYLINDRICAL_SURFACE('',#16415,0.605);
#12422=CYLINDRICAL_SURFACE('',#16418,0.8);
#13230=ADVANCED_FACE('',(#2863),#12421,.F.);
#13231=ADVANCED_FACE('',(#2864),#12422,.T.);
#13232=ADVANCED_FACE('',(#2865,#1631),#2054,.T.);
#13233=ADVANCED_FACE('',(#2866,#1632),#2055,.F.);
#13370=CLOSED_SHELL('',(#13230,#13231,#13232,#13233));
#16414=AXIS2_PLACEMENT_3D('',#24778,#20857,#20858);
#16415=AXIS2_PLACEMENT_3D('',#24779,#20859,#20860);
#16416=AXIS2_PLACEMENT_3D('',#24781,#20861,#20862);
#16417=AXIS2_PLACEMENT_3D('',#24784,#20864,#20865);
#16418=AXIS2_PLACEMENT_3D('',#24785,#20866,#20867);
#16419=AXIS2_PLACEMENT_3D('',#24787,#20868,#20869);
#16420=AXIS2_PLACEMENT_3D('',#24790,#20871,#20872);
#16421=AXIS2_PLACEMENT_3D('',#24791,#20873,#20874);
#16422=AXIS2_PLACEMENT_3D('',#24792,#20875,#20876);
#20857=DIRECTION('axis',(0.,0.,1.));
#20858=DIRECTION('refdir',(1.,0.,0.));
#20859=DIRECTION('center_axis',(1.,0.,0.));
#20860=DIRECTION('ref_axis',(0.,0.,-1.));
#20861=DIRECTION('center_axis',(-1.,0.,0.));
#20862=DIRECTION('ref_axis',(0.,0.,-1.));
#20863=DIRECTION('',(-1.,0.,0.));
#20864=DIRECTION('center_axis',(-1.,0.,0.));
#20865=DIRECTION('ref_axis',(0.,0.,-1.));
#20866=DIRECTION('center_axis',(1.,0.,0.));
#20867=DIRECTION('ref_axis',(0.,0.,-1.));
#20868=DIRECTION('center_axis',(1.,0.,0.));
#20869=DIRECTION('ref_axis',(0.,0.,-1.));
#20870=DIRECTION('',(-1.,0.,0.));
#20871=DIRECTION('center_axis',(1.,0.,0.));
#20872=DIRECTION('ref_axis',(0.,0.,-1.));
#20873=DIRECTION('center_axis',(1.,0.,0.));
#20874=DIRECTION('ref_axis',(0.,0.,-1.));
#20875=DIRECTION('center_axis',(1.,0.,0.));
#20876=DIRECTION('ref_axis',(0.,0.,-1.));
#24778=CARTESIAN_POINT('',(0.,0.,0.));
#24779=CARTESIAN_POINT('Origin',(45.5,0.,6.));
#24780=CARTESIAN_POINT('',(46.3,-7.40911313484149E-17,6.605));
#24781=CARTESIAN_POINT('Origin',(46.3,0.,6.));
#24782=CARTESIAN_POINT('',(45.5,-7.40911313484149E-17,6.605));
#24783=CARTESIAN_POINT('',(45.5,-7.40911313484149E-17,6.605));
#24784=CARTESIAN_POINT('Origin',(45.5,0.,6.));
#24785=CARTESIAN_POINT('Origin',(45.5,0.,6.));
#24786=CARTESIAN_POINT('',(46.3,-9.79717439317882E-17,6.8));
#24787=CARTESIAN_POINT('Origin',(46.3,0.,6.));
#24788=CARTESIAN_POINT('',(45.5,-9.79717439317882E-17,6.8));
#24789=CARTESIAN_POINT('',(45.5,-9.79717439317882E-17,6.8));
#24790=CARTESIAN_POINT('Origin',(45.5,0.,6.));
#24791=CARTESIAN_POINT('Origin',(46.3,0.,6.));
#24792=CARTESIAN_POINT('Origin',(45.5,0.,6.));
#24975=UNCERTAINTY_MEASURE_WITH_UNIT(LENGTH_MEASURE(0.001),#25101,
'DISTANCE_ACCURACY_VALUE',
'Maximum model space distance between geometric entities at asserted c
onnectivities');
#24979=UNCERTAINTY_MEASURE_WITH_UNIT(LENGTH_MEASURE(0.001),#25101,
'DISTANCE_ACCURACY_VALUE',
'Maximum model space distance between geometric entities at asserted c
onnectivities');
#25096=(
GEOMETRIC_REPRESENTATION_CONTEXT(3)
GLOBAL_UNCERTAINTY_ASSIGNED_CONTEXT((#24975))
GLOBAL_UNIT_ASSIGNED_CONTEXT((#25101,#25103,#25104))
REPRESENTATION_CONTEXT('','3D')
);
#25100=(
GEOMETRIC_REPRESENTATION_CONTEXT(3)
GLOBAL_UNCERTAINTY_ASSIGNED_CONTEXT((#24979))
GLOBAL_UNIT_ASSIGNED_CONTEXT((#25101,#25103,#25104))
REPRESENTATION_CONTEXT('','3D')
);
#25101=(
LENGTH_UNIT()
NAMED_UNIT(*)
SI_UNIT(.CENTI.,.METRE.)
);
#25103=(
NAMED_UNIT(*)
PLANE_ANGLE_UNIT()
SI_UNIT($,.RADIAN.)
);
#25104=(
NAMED_UNIT(*)
SI_UNIT($,.STERADIAN.)
SOLID_ANGLE_UNIT()
);
#25221=SHAPE_DEFINITION_REPRESENTATION(#25493,#25626);
#25493=PRODUCT_DEFINITION_SHAPE('',$,#25747);
#25626=SHAPE_REPRESENTATION('',(#16414),#25096);
#25630=PRODUCT_DEFINITION_CONTEXT('part definition',#25992,'design');
#25747=PRODUCT_DEFINITION('Bearing inner spacer (1)',
'Bearing inner spacer (1)',#25867,#25630);
#25867=PRODUCT_DEFINITION_FORMATION('',$,#26110);
#25992=APPLICATION_CONTEXT(
'Core Data for Automotive Mechanical Design Process');
#25993=PRODUCT_CONTEXT('part definition',#25992,'mechanical');
#26110=PRODUCT('Bearing inner spacer (1)','Bearing inner spacer (1)',
'Bearing inner spacer (1)',(#25993));
#26185=COLOUR_RGB('Grey',0.48,0.52,0.57);
#26186=FILL_AREA_STYLE_COLOUR('',#26185);
#26187=FILL_AREA_STYLE('',(#26186));
#26188=SURFACE_STYLE_FILL_AREA(#26187);
#26189=SURFACE_SIDE_STYLE('',(#26188));
#26190=SURFACE_STYLE_USAGE(.BOTH.,#26189);
#26191=PRESENTATION_STYLE_ASSIGNMENT((#26190));
ENDSEC;
END-ISO-10303-21;
